ISO-10303-21;
HEADER;
/* Generated by software containing ST-Developer
 * from STEP Tools, Inc. (www.steptools.com) 
 */

FILE_DESCRIPTION(
/* description */ ('STEP AP214'),
/* implementation_level */ '2;1');

FILE_NAME(
/* name */ 'Ball Screw Spacer 2.step',
/* time_stamp */ '2026-11-15T14:49:54-08:00',
/* author */ (''),
/* organization */ (''),
/* preprocessor_version */ 'ST-DEVELOPER v20.2',
/* originating_system */ 'Autodesk Translation Framework v15.17.0.0',
/* authorisation */ '');

FILE_SCHEMA (('AUTOMOTIVE_DESIGN { 1 0 10303 214 3 1 1 }'));
ENDSEC;

DATA;
#10=MECHANICAL_DESIGN_GEOMETRIC_PRESENTATION_REPRESENTATION('',(#1099),#66721);
#1037=SHAPE_REPRESENTATION_RELATIONSHIP('SRR','None',#66893,#1068);
#1068=ADVANCED_BREP_SHAPE_REPRESENTATION('',(#1134),#66684);
#1099=STYLED_ITEM('',(#67095),#1134);
#1134=MANIFOLD_SOLID_BREP('Body1',#25665);
#1180=FACE_BOUND('',#3752,.T.);
#1181=FACE_BOUND('',#3753,.T.);
#1182=FACE_BOUND('',#3754,.T.);
#1183=FACE_BOUND('',#3755,.T.);
#1184=FACE_BOUND('',#3761,.T.);
#1185=FACE_BOUND('',#3762,.T.);
#1186=FACE_BOUND('',#3763,.T.);
#1187=FACE_BOUND('',#3764,.T.);
#1512=PLANE('',#26083);
#1513=PLANE('',#26084);
#1514=PLANE('',#26085);
#1515=PLANE('',#26086);
#1516=PLANE('',#26087);
#1517=PLANE('',#26088);
#1518=PLANE('',#26089);
#1519=PLANE('',#26090);
#1520=PLANE('',#26091);
#1521=PLANE('',#26092);
#1522=PLANE('',#26093);
#1523=PLANE('',#26094);
#2287=FACE_OUTER_BOUND('',#3741,.T.);
#2288=FACE_OUTER_BOUND('',#3742,.T.);
#2289=FACE_OUTER_BOUND('',#3743,.T.);
#2290=FACE_OUTER_BOUND('',#3744,.T.);
#2291=FACE_OUTER_BOUND('',#3745,.T.);
#2292=FACE_OUTER_BOUND('',#3746,.T.);
#2293=FACE_OUTER_BOUND('',#3747,.T.);
#2294=FACE_OUTER_BOUND('',#3748,.T.);
#2295=FACE_OUTER_BOUND('',#3749,.T.);
#2296=FACE_OUTER_BOUND('',#3750,.T.);
#2297=FACE_OUTER_BOUND('',#3751,.T.);
#2298=FACE_OUTER_BOUND('',#3756,.T.);
#2299=FACE_OUTER_BOUND('',#3757,.T.);
#2300=FACE_OUTER_BOUND('',#3758,.T.);
#2301=FACE_OUTER_BOUND('',#3759,.T.);
#2302=FACE_OUTER_BOUND('',#3760,.T.);
#3741=EDGE_LOOP('',(#16690,#16691,#16692,#16693));
#3742=EDGE_LOOP('',(#16694,#16695,#16696,#16697));
#3743=EDGE_LOOP('',(#16698,#16699,#16700,#16701));
#3744=EDGE_LOOP('',(#16702,#16703,#16704,#16705));
#3745=EDGE_LOOP('',(#16706,#16707,#16708,#16709));
#3746=EDGE_LOOP('',(#16710,#16711,#16712,#16713,#16714,#16715));
#3747=EDGE_LOOP('',(#16716,#16717,#16718,#16719,#16720,#16721));
#3748=EDGE_LOOP('',(#16722,#16723,#16724,#16725,#16726,#16727));
#3749=EDGE_LOOP('',(#16728,#16729,#16730,#16731,#16732,#16733));
#3750=EDGE_LOOP('',(#16734,#16735,#16736,#16737));
#3751=EDGE_LOOP('',(#16738,#16739,#16740,#16741));
#3752=EDGE_LOOP('',(#16742));
#3753=EDGE_LOOP('',(#16743));
#3754=EDGE_LOOP('',(#16744));
#3755=EDGE_LOOP('',(#16745));
#3756=EDGE_LOOP('',(#16746,#16747,#16748,#16749));
#3757=EDGE_LOOP('',(#16750,#16751,#16752,#16753));
#3758=EDGE_LOOP('',(#16754,#16755,#16756,#16757));
#3759=EDGE_LOOP('',(#16758,#16759,#16760,#16761));
#3760=EDGE_LOOP('',(#16762,#16763,#16764,#16765,#16766,#16767,#16768,#16769));
#3761=EDGE_LOOP('',(#16770));
#3762=EDGE_LOOP('',(#16771));
#3763=EDGE_LOOP('',(#16772));
#3764=EDGE_LOOP('',(#16773));
#5523=LINE('',#36281,#7512);
#5524=LINE('',#36287,#7513);
#5525=LINE('',#36293,#7514);
#5526=LINE('',#36299,#7515);
#5527=LINE('',#36304,#7516);
#5528=LINE('',#36306,#7517);
#5529=LINE('',#36308,#7518);
#5530=LINE('',#36309,#7519);
#5531=LINE('',#36312,#7520);
#5532=LINE('',#36314,#7521);
#5533=LINE('',#36316,#7522);
#5534=LINE('',#36318,#7523);
#5535=LINE('',#36319,#7524);
#5536=LINE('',#36323,#7525);
#5537=LINE('',#36324,#7526);
#5538=LINE('',#36326,#7527);
#5539=LINE('',#36327,#7528);
#5540=LINE('',#36331,#7529);
#5541=LINE('',#36333,#7530);
#5542=LINE('',#36334,#7531);
#5543=LINE('',#36336,#7532);
#5544=LINE('',#36337,#7533);
#5545=LINE('',#36340,#7534);
#5546=LINE('',#36342,#7535);
#5547=LINE('',#36343,#7536);
#5548=LINE('',#36344,#7537);
#5549=LINE('',#36347,#7538);
#5550=LINE('',#36348,#7539);
#5551=LINE('',#36352,#7540);
#5552=LINE('',#36353,#7541);
#5553=LINE('',#36355,#7542);
#5554=LINE('',#36358,#7543);
#5555=LINE('',#36359,#7544);
#5556=LINE('',#36361,#7545);
#7512=VECTOR('',#28860,3.);
#7513=VECTOR('',#28867,3.);
#7514=VECTOR('',#28874,4.25000000000001);
#7515=VECTOR('',#28881,4.25000000000001);
#7516=VECTOR('',#28886,1000.);
#7517=VECTOR('',#28887,1000.);
#7518=VECTOR('',#28888,1000.);
#7519=VECTOR('',#28889,1000.);
#7520=VECTOR('',#28892,1000.);
#7521=VECTOR('',#28893,1000.);
#7522=VECTOR('',#28894,1000.);
#7523=VECTOR('',#28895,1000.);
#7524=VECTOR('',#28896,1000.);
#7525=VECTOR('',#28899,1000.);
#7526=VECTOR('',#28900,1000.);
#7527=VECTOR('',#28901,1000.);
#7528=VECTOR('',#28902,1000.);
#7529=VECTOR('',#28905,1000.);
#7530=VECTOR('',#28906,1000.);
#7531=VECTOR('',#28907,1000.);
#7532=VECTOR('',#28908,1000.);
#7533=VECTOR('',#28909,1000.);
#7534=VECTOR('',#28912,1000.);
#7535=VECTOR('',#28913,1000.);
#7536=VECTOR('',#28914,1000.);
#7537=VECTOR('',#28915,1000.);
#7538=VECTOR('',#28918,1000.);
#7539=VECTOR('',#28919,1000.);
#7540=VECTOR('',#28924,1000.);
#7541=VECTOR('',#28925,1000.);
#7542=VECTOR('',#28928,1000.);
#7543=VECTOR('',#28931,1000.);
#7544=VECTOR('',#28932,1000.);
#7545=VECTOR('',#28935,1000.);
#9469=CIRCLE('',#26072,3.);
#9470=CIRCLE('',#26073,3.);
#9471=CIRCLE('',#26075,3.);
#9472=CIRCLE('',#26076,3.);
#9473=CIRCLE('',#26078,4.25000000000001);
#9474=CIRCLE('',#26079,4.25000000000001);
#9475=CIRCLE('',#26081,4.25000000000001);
#9476=CIRCLE('',#26082,4.25000000000001);
#10670=VERTEX_POINT('',#36278);
#10671=VERTEX_POINT('',#36280);
#10672=VERTEX_POINT('',#36284);
#10673=VERTEX_POINT('',#36286);
#10674=VERTEX_POINT('',#36290);
#10675=VERTEX_POINT('',#36292);
#10676=VERTEX_POINT('',#36296);
#10677=VERTEX_POINT('',#36298);
#10678=VERTEX_POINT('',#36302);
#10679=VERTEX_POINT('',#36303);
#10680=VERTEX_POINT('',#36305);
#10681=VERTEX_POINT('',#36307);
#10682=VERTEX_POINT('',#36311);
#10683=VERTEX_POINT('',#36313);
#10684=VERTEX_POINT('',#36315);
#10685=VERTEX_POINT('',#36317);
#10686=VERTEX_POINT('',#36321);
#10687=VERTEX_POINT('',#36322);
#10688=VERTEX_POINT('',#36325);
#10689=VERTEX_POINT('',#36329);
#10690=VERTEX_POINT('',#36330);
#10691=VERTEX_POINT('',#36332);
#10692=VERTEX_POINT('',#36335);
#10693=VERTEX_POINT('',#36339);
#10694=VERTEX_POINT('',#36341);
#10695=VERTEX_POINT('',#36346);
#10696=VERTEX_POINT('',#36351);
#10697=VERTEX_POINT('',#36357);
#13038=EDGE_CURVE('',#10670,#10670,#9469,.T.);
#13039=EDGE_CURVE('',#10670,#10671,#5523,.T.);
#13040=EDGE_CURVE('',#10671,#10671,#9470,.T.);
#13041=EDGE_CURVE('',#10672,#10672,#9471,.T.);
#13042=EDGE_CURVE('',#10672,#10673,#5524,.T.);
#13043=EDGE_CURVE('',#10673,#10673,#9472,.T.);
#13044=EDGE_CURVE('',#10674,#10674,#9473,.T.);
#13045=EDGE_CURVE('',#10674,#10675,#5525,.T.);
#13046=EDGE_CURVE('',#10675,#10675,#9474,.T.);
#13047=EDGE_CURVE('',#10676,#10676,#9475,.T.);
#13048=EDGE_CURVE('',#10676,#10677,#5526,.T.);
#13049=EDGE_CURVE('',#10677,#10677,#9476,.T.);
#13050=EDGE_CURVE('',#10678,#10679,#5527,.T.);
#13051=EDGE_CURVE('',#10680,#10678,#5528,.T.);
#13052=EDGE_CURVE('',#10680,#10681,#5529,.T.);
#13053=EDGE_CURVE('',#10681,#10679,#5530,.T.);
#13054=EDGE_CURVE('',#10682,#10680,#5531,.T.);
#13055=EDGE_CURVE('',#10683,#10682,#5532,.T.);
#13056=EDGE_CURVE('',#10683,#10684,#5533,.T.);
#13057=EDGE_CURVE('',#10684,#10685,#5534,.T.);
#13058=EDGE_CURVE('',#10681,#10685,#5535,.T.);
#13059=EDGE_CURVE('',#10686,#10687,#5536,.T.);
#13060=EDGE_CURVE('',#10686,#10679,#5537,.T.);
#13061=EDGE_CURVE('',#10685,#10688,#5538,.T.);
#13062=EDGE_CURVE('',#10687,#10688,#5539,.T.);
#13063=EDGE_CURVE('',#10689,#10690,#5540,.T.);
#13064=EDGE_CURVE('',#10691,#10689,#5541,.T.);
#13065=EDGE_CURVE('',#10687,#10691,#5542,.T.);
#13066=EDGE_CURVE('',#10688,#10692,#5543,.T.);
#13067=EDGE_CURVE('',#10690,#10692,#5544,.T.);
#13068=EDGE_CURVE('',#10693,#10683,#5545,.T.);
#13069=EDGE_CURVE('',#10693,#10694,#5546,.T.);
#13070=EDGE_CURVE('',#10690,#10694,#5547,.T.);
#13071=EDGE_CURVE('',#10692,#10684,#5548,.T.);
#13072=EDGE_CURVE('',#10695,#10694,#5549,.T.);
#13073=EDGE_CURVE('',#10689,#10695,#5550,.T.);
#13074=EDGE_CURVE('',#10696,#10686,#5551,.T.);
#13075=EDGE_CURVE('',#10696,#10678,#5552,.T.);
#13076=EDGE_CURVE('',#10682,#10696,#5553,.T.);
#13077=EDGE_CURVE('',#10697,#10693,#5554,.T.);
#13078=EDGE_CURVE('',#10697,#10695,#5555,.T.);
#13079=EDGE_CURVE('',#10691,#10697,#5556,.T.);
#16690=ORIENTED_EDGE('',*,*,#13038,.F.);
#16691=ORIENTED_EDGE('',*,*,#13039,.T.);
#16692=ORIENTED_EDGE('',*,*,#13040,.T.);
#16693=ORIENTED_EDGE('',*,*,#13039,.F.);
#16694=ORIENTED_EDGE('',*,*,#13041,.F.);
#16695=ORIENTED_EDGE('',*,*,#13042,.T.);
#16696=ORIENTED_EDGE('',*,*,#13043,.T.);
#16697=ORIENTED_EDGE('',*,*,#13042,.F.);
#16698=ORIENTED_EDGE('',*,*,#13044,.F.);
#16699=ORIENTED_EDGE('',*,*,#13045,.T.);
#16700=ORIENTED_EDGE('',*,*,#13046,.T.);
#16701=ORIENTED_EDGE('',*,*,#13045,.F.);
#16702=ORIENTED_EDGE('',*,*,#13047,.F.);
#16703=ORIENTED_EDGE('',*,*,#13048,.T.);
#16704=ORIENTED_EDGE('',*,*,#13049,.T.);
#16705=ORIENTED_EDGE('',*,*,#13048,.F.);
#16706=ORIENTED_EDGE('',*,*,#13050,.F.);
#16707=ORIENTED_EDGE('',*,*,#13051,.F.);
#16708=ORIENTED_EDGE('',*,*,#13052,.T.);
#16709=ORIENTED_EDGE('',*,*,#13053,.T.);
#16710=ORIENTED_EDGE('',*,*,#13052,.F.);
#16711=ORIENTED_EDGE('',*,*,#13054,.F.);
#16712=ORIENTED_EDGE('',*,*,#13055,.F.);
#16713=ORIENTED_EDGE('',*,*,#13056,.T.);
#16714=ORIENTED_EDGE('',*,*,#13057,.T.);
#16715=ORIENTED_EDGE('',*,*,#13058,.F.);
#16716=ORIENTED_EDGE('',*,*,#13059,.F.);
#16717=ORIENTED_EDGE('',*,*,#13060,.T.);
#16718=ORIENTED_EDGE('',*,*,#13053,.F.);
#16719=ORIENTED_EDGE('',*,*,#13058,.T.);
#16720=ORIENTED_EDGE('',*,*,#13061,.T.);
#16721=ORIENTED_EDGE('',*,*,#13062,.F.);
#16722=ORIENTED_EDGE('',*,*,#13063,.F.);
#16723=ORIENTED_EDGE('',*,*,#13064,.F.);
#16724=ORIENTED_EDGE('',*,*,#13065,.F.);
#16725=ORIENTED_EDGE('',*,*,#13062,.T.);
#16726=ORIENTED_EDGE('',*,*,#13066,.T.);
#16727=ORIENTED_EDGE('',*,*,#13067,.F.);
#16728=ORIENTED_EDGE('',*,*,#13068,.F.);
#16729=ORIENTED_EDGE('',*,*,#13069,.T.);
#16730=ORIENTED_EDGE('',*,*,#13070,.F.);
#16731=ORIENTED_EDGE('',*,*,#13067,.T.);
#16732=ORIENTED_EDGE('',*,*,#13071,.T.);
#16733=ORIENTED_EDGE('',*,*,#13056,.F.);
#16734=ORIENTED_EDGE('',*,*,#13072,.F.);
#16735=ORIENTED_EDGE('',*,*,#13073,.F.);
#16736=ORIENTED_EDGE('',*,*,#13063,.T.);
#16737=ORIENTED_EDGE('',*,*,#13070,.T.);
#16738=ORIENTED_EDGE('',*,*,#13057,.F.);
#16739=ORIENTED_EDGE('',*,*,#13071,.F.);
#16740=ORIENTED_EDGE('',*,*,#13066,.F.);
#16741=ORIENTED_EDGE('',*,*,#13061,.F.);
#16742=ORIENTED_EDGE('',*,*,#13038,.T.);
#16743=ORIENTED_EDGE('',*,*,#13041,.T.);
#16744=ORIENTED_EDGE('',*,*,#13044,.T.);
#16745=ORIENTED_EDGE('',*,*,#13047,.T.);
#16746=ORIENTED_EDGE('',*,*,#13050,.T.);
#16747=ORIENTED_EDGE('',*,*,#13060,.F.);
#16748=ORIENTED_EDGE('',*,*,#13074,.F.);
#16749=ORIENTED_EDGE('',*,*,#13075,.T.);
#16750=ORIENTED_EDGE('',*,*,#13051,.T.);
#16751=ORIENTED_EDGE('',*,*,#13075,.F.);
#16752=ORIENTED_EDGE('',*,*,#13076,.F.);
#16753=ORIENTED_EDGE('',*,*,#13054,.T.);
#16754=ORIENTED_EDGE('',*,*,#13072,.T.);
#16755=ORIENTED_EDGE('',*,*,#13069,.F.);
#16756=ORIENTED_EDGE('',*,*,#13077,.F.);
#16757=ORIENTED_EDGE('',*,*,#13078,.T.);
#16758=ORIENTED_EDGE('',*,*,#13073,.T.);
#16759=ORIENTED_EDGE('',*,*,#13078,.F.);
#16760=ORIENTED_EDGE('',*,*,#13079,.F.);
#16761=ORIENTED_EDGE('',*,*,#13064,.T.);
#16762=ORIENTED_EDGE('',*,*,#13065,.T.);
#16763=ORIENTED_EDGE('',*,*,#13079,.T.);
#16764=ORIENTED_EDGE('',*,*,#13077,.T.);
#16765=ORIENTED_EDGE('',*,*,#13068,.T.);
#16766=ORIENTED_EDGE('',*,*,#13055,.T.);
#16767=ORIENTED_EDGE('',*,*,#13076,.T.);
#16768=ORIENTED_EDGE('',*,*,#13074,.T.);
#16769=ORIENTED_EDGE('',*,*,#13059,.T.);
#16770=ORIENTED_EDGE('',*,*,#13040,.F.);
#16771=ORIENTED_EDGE('',*,*,#13043,.F.);
#16772=ORIENTED_EDGE('',*,*,#13046,.F.);
#16773=ORIENTED_EDGE('',*,*,#13049,.F.);
#23806=CYLINDRICAL_SURFACE('',#26071,3.);
#23807=CYLINDRICAL_SURFACE('',#26074,3.);
#23808=CYLINDRICAL_SURFACE('',#26077,4.25000000000001);
#23809=CYLINDRICAL_SURFACE('',#26080,4.25000000000001);
#24240=ADVANCED_FACE('',(#2287),#23806,.F.);
#24241=ADVANCED_FACE('',(#2288),#23807,.F.);
#24242=ADVANCED_FACE('',(#2289),#23808,.F.);
#24243=ADVANCED_FACE('',(#2290),#23809,.F.);
#24244=ADVANCED_FACE('',(#2291),#1512,.T.);
#24245=ADVANCED_FACE('',(#2292),#1513,.F.);
#24246=ADVANCED_FACE('',(#2293),#1514,.F.);
#24247=ADVANCED_FACE('',(#2294),#1515,.F.);
#24248=ADVANCED_FACE('',(#2295),#1516,.F.);
#24249=ADVANCED_FACE('',(#2296),#1517,.T.);
#24250=ADVANCED_FACE('',(#2297,#1180,#1181,#1182,#1183),#1518,.F.);
#24251=ADVANCED_FACE('',(#2298),#1519,.F.);
#24252=ADVANCED_FACE('',(#2299),#1520,.F.);
#24253=ADVANCED_FACE('',(#2300),#1521,.F.);
#24254=ADVANCED_FACE('',(#2301),#1522,.F.);
#24255=ADVANCED_FACE('',(#2302,#1184,#1185,#1186,#1187),#1523,.T.);
#25665=CLOSED_SHELL('',(#24240,#24241,#24242,#24243,#24244,#24245,#24246,
#24247,#24248,#24249,#24250,#24251,#24252,#24253,#24254,#24255));
#26070=AXIS2_PLACEMENT_3D('',#36276,#28854,#28855);
#26071=AXIS2_PLACEMENT_3D('',#36277,#28856,#28857);
#26072=AXIS2_PLACEMENT_3D('',#36279,#28858,#28859);
#26073=AXIS2_PLACEMENT_3D('',#36282,#28861,#28862);
#26074=AXIS2_PLACEMENT_3D('',#36283,#28863,#28864);
#26075=AXIS2_PLACEMENT_3D('',#36285,#28865,#28866);
#26076=AXIS2_PLACEMENT_3D('',#36288,#28868,#28869);
#26077=AXIS2_PLACEMENT_3D('',#36289,#28870,#28871);
#26078=AXIS2_PLACEMENT_3D('',#36291,#28872,#28873);
#26079=AXIS2_PLACEMENT_3D('',#36294,#28875,#28876);
#26080=AXIS2_PLACEMENT_3D('',#36295,#28877,#28878);
#26081=AXIS2_PLACEMENT_3D('',#36297,#28879,#28880);
#26082=AXIS2_PLACEMENT_3D('',#36300,#28882,#28883);
#26083=AXIS2_PLACEMENT_3D('',#36301,#28884,#28885);
#26084=AXIS2_PLACEMENT_3D('',#36310,#28890,#28891);
#26085=AXIS2_PLACEMENT_3D('',#36320,#28897,#28898);
#26086=AXIS2_PLACEMENT_3D('',#36328,#28903,#28904);
#26087=AXIS2_PLACEMENT_3D('',#36338,#28910,#28911);
#26088=AXIS2_PLACEMENT_3D('',#36345,#28916,#28917);
#26089=AXIS2_PLACEMENT_3D('',#36349,#28920,#28921);
#26090=AXIS2_PLACEMENT_3D('',#36350,#28922,#28923);
#26091=AXIS2_PLACEMENT_3D('',#36354,#28926,#28927);
#26092=AXIS2_PLACEMENT_3D('',#36356,#28929,#28930);
#26093=AXIS2_PLACEMENT_3D('',#36360,#28933,#28934);
#26094=AXIS2_PLACEMENT_3D('',#36362,#28936,#28937);
#28854=DIRECTION('axis',(0.,0.,1.));
#28855=DIRECTION('refdir',(1.,0.,0.));
#28856=DIRECTION('center_axis',(0.,0.,1.));
#28857=DIRECTION('ref_axis',(1.,0.,0.));
#28858=DIRECTION('center_axis',(0.,0.,1.));
#28859=DIRECTION('ref_axis',(1.,0.,0.));
#28860=DIRECTION('',(0.,0.,1.));
#28861=DIRECTION('center_axis',(0.,0.,1.));
#28862=DIRECTION('ref_axis',(1.,0.,0.));
#28863=DIRECTION('center_axis',(0.,0.,1.));
#28864=DIRECTION('ref_axis',(1.,0.,0.));
#28865=DIRECTION('center_axis',(0.,0.,1.));
#28866=DIRECTION('ref_axis',(1.,0.,0.));
#28867=DIRECTION('',(0.,0.,1.));
#28868=DIRECTION('center_axis',(0.,0.,1.));
#28869=DIRECTION('ref_axis',(1.,0.,0.));
#28870=DIRECTION('center_axis',(0.,0.,1.));
#28871=DIRECTION('ref_axis',(1.,0.,0.));
#28872=DIRECTION('center_axis',(0.,0.,1.));
#28873=DIRECTION('ref_axis',(1.,0.,0.));
#28874=DIRECTION('',(0.,0.,1.));
#28875=DIRECTION('center_axis',(0.,0.,1.));
#28876=DIRECTION('ref_axis',(1.,0.,0.));
#28877=DIRECTION('center_axis',(0.,0.,1.));
#28878=DIRECTION('ref_axis',(1.,0.,0.));
#28879=DIRECTION('center_axis',(0.,0.,1.));
#28880=DIRECTION('ref_axis',(1.,0.,0.));
#28881=DIRECTION('',(0.,0.,1.));
#28882=DIRECTION('center_axis',(0.,0.,1.));
#28883=DIRECTION('ref_axis',(1.,0.,0.));
#28884=DIRECTION('center_axis',(0.,0.,1.));
#28885=DIRECTION('ref_axis',(1.,0.,0.));
#28886=DIRECTION('',(-5.33761069531325E-16,1.,0.));
#28887=DIRECTION('',(-1.,0.,0.));
#28888=DIRECTION('',(0.,1.,0.));
#28889=DIRECTION('',(-1.,0.,0.));
#28890=DIRECTION('center_axis',(-1.,0.,0.));
#28891=DIRECTION('ref_axis',(0.,0.,1.));
#28892=DIRECTION('',(0.,0.,1.));
#28893=DIRECTION('',(6.93889390390723E-16,1.,0.));
#28894=DIRECTION('',(0.,0.,-1.));
#28895=DIRECTION('',(0.,1.,0.));
#28896=DIRECTION('',(0.,0.,-1.));
#28897=DIRECTION('center_axis',(0.,-1.,0.));
#28898=DIRECTION('ref_axis',(0.,0.,-1.));
#28899=DIRECTION('',(-1.,0.,0.));
#28900=DIRECTION('',(0.,0.,1.));
#28901=DIRECTION('',(-1.,0.,0.));
#28902=DIRECTION('',(0.,0.,-1.));
#28903=DIRECTION('center_axis',(1.,0.,0.));
#28904=DIRECTION('ref_axis',(0.,0.,-1.));
#28905=DIRECTION('',(0.,-1.,0.));
#28906=DIRECTION('',(0.,0.,1.));
#28907=DIRECTION('',(0.,-1.,0.));
#28908=DIRECTION('',(0.,-1.,0.));
#28909=DIRECTION('',(0.,0.,-1.));
#28910=DIRECTION('center_axis',(0.,1.,0.));
#28911=DIRECTION('ref_axis',(0.,0.,1.));
#28912=DIRECTION('',(1.,-8.67361737988404E-17,0.));
#28913=DIRECTION('',(0.,0.,1.));
#28914=DIRECTION('',(1.,0.,0.));
#28915=DIRECTION('',(1.,0.,0.));
#28916=DIRECTION('center_axis',(0.,0.,1.));
#28917=DIRECTION('ref_axis',(1.,0.,0.));
#28918=DIRECTION('',(0.,-1.,0.));
#28919=DIRECTION('',(1.,0.,0.));
#28920=DIRECTION('center_axis',(0.,0.,1.));
#28921=DIRECTION('ref_axis',(1.,0.,0.));
#28922=DIRECTION('center_axis',(1.,5.33761069531325E-16,0.));
#28923=DIRECTION('ref_axis',(-5.33761069531325E-16,1.,0.));
#28924=DIRECTION('',(-5.33761069531325E-16,1.,0.));
#28925=DIRECTION('',(0.,0.,1.));
#28926=DIRECTION('center_axis',(0.,1.,0.));
#28927=DIRECTION('ref_axis',(0.,0.,1.));
#28928=DIRECTION('',(-1.,0.,0.));
#28929=DIRECTION('center_axis',(-1.,0.,0.));
#28930=DIRECTION('ref_axis',(0.,0.,1.));
#28931=DIRECTION('',(0.,-1.,0.));
#28932=DIRECTION('',(0.,0.,1.));
#28933=DIRECTION('center_axis',(0.,-1.,0.));
#28934=DIRECTION('ref_axis',(0.,0.,-1.));
#28935=DIRECTION('',(1.,0.,0.));
#28936=DIRECTION('center_axis',(0.,0.,1.));
#28937=DIRECTION('ref_axis',(1.,0.,0.));
#36276=CARTESIAN_POINT('',(0.,0.,0.));
#36277=CARTESIAN_POINT('Origin',(-13.5,0.5,1.));
#36278=CARTESIAN_POINT('',(-16.5,0.5,-4.));
#36279=CARTESIAN_POINT('Origin',(-13.5,0.5,-4.));
#36280=CARTESIAN_POINT('',(-16.5,0.5,1.));
#36281=CARTESIAN_POINT('',(-16.5,0.5,1.));
#36282=CARTESIAN_POINT('Origin',(-13.5,0.5,1.));
#36283=CARTESIAN_POINT('Origin',(11.5,0.5,1.));
#36284=CARTESIAN_POINT('',(8.5,0.5,-4.));
#36285=CARTESIAN_POINT('Origin',(11.5,0.5,-4.));
#36286=CARTESIAN_POINT('',(8.5,0.5,1.));
#36287=CARTESIAN_POINT('',(8.5,0.5,1.));
#36288=CARTESIAN_POINT('Origin',(11.5,0.5,1.));
#36289=CARTESIAN_POINT('Origin',(-27.,0.5,-4.));
#36290=CARTESIAN_POINT('',(-31.25,0.499999999999999,-4.));
#36291=CARTESIAN_POINT('Origin',(-27.,0.5,-4.));
#36292=CARTESIAN_POINT('',(-31.25,0.499999999999999,1.));
#36293=CARTESIAN_POINT('',(-31.25,0.499999999999999,-4.));
#36294=CARTESIAN_POINT('Origin',(-27.,0.5,1.));
#36295=CARTESIAN_POINT('Origin',(25.,0.5,-4.));
#36296=CARTESIAN_POINT('',(20.75,0.499999999999999,-4.));
#36297=CARTESIAN_POINT('Origin',(25.,0.5,-4.));
#36298=CARTESIAN_POINT('',(20.75,0.499999999999999,1.));
#36299=CARTESIAN_POINT('',(20.75,0.499999999999999,-4.));
#36300=CARTESIAN_POINT('Origin',(25.,0.5,1.));
#36301=CARTESIAN_POINT('Origin',(0.,0.,4.));
#36302=CARTESIAN_POINT('',(34.,-1.5,4.));
#36303=CARTESIAN_POINT('',(34.,11.5,4.));
#36304=CARTESIAN_POINT('',(34.,11.5,4.));
#36305=CARTESIAN_POINT('',(36.5,-1.5,4.));
#36306=CARTESIAN_POINT('',(34.,-1.5,4.));
#36307=CARTESIAN_POINT('',(36.5,11.5,4.));
#36308=CARTESIAN_POINT('',(36.5,11.5,4.));
#36309=CARTESIAN_POINT('',(-36.5,11.5,4.));
#36310=CARTESIAN_POINT('Origin',(36.5,11.5,4.));
#36311=CARTESIAN_POINT('',(36.5,-1.5,1.));
#36312=CARTESIAN_POINT('',(36.5,-1.5,1.));
#36313=CARTESIAN_POINT('',(36.5,-11.5,1.));
#36314=CARTESIAN_POINT('',(36.5,-11.5,1.));
#36315=CARTESIAN_POINT('',(36.5,-11.5,-4.));
#36316=CARTESIAN_POINT('',(36.5,-11.5,4.));
#36317=CARTESIAN_POINT('',(36.5,11.5,-4.));
#36318=CARTESIAN_POINT('',(36.5,11.5,-4.));
#36319=CARTESIAN_POINT('',(36.5,11.5,4.));
#36320=CARTESIAN_POINT('Origin',(-36.5,11.5,4.));
#36321=CARTESIAN_POINT('',(34.,11.5,1.));
#36322=CARTESIAN_POINT('',(-36.5,11.5,1.));
#36323=CARTESIAN_POINT('',(-36.5,11.5,1.));
#36324=CARTESIAN_POINT('',(34.,11.5,1.));
#36325=CARTESIAN_POINT('',(-36.5,11.5,-4.));
#36326=CARTESIAN_POINT('',(-36.5,11.5,-4.));
#36327=CARTESIAN_POINT('',(-36.5,11.5,4.));
#36328=CARTESIAN_POINT('Origin',(-36.5,11.5,4.));
#36329=CARTESIAN_POINT('',(-36.5,-9.5,4.));
#36330=CARTESIAN_POINT('',(-36.5,-11.5,4.));
#36331=CARTESIAN_POINT('',(-36.5,11.5,4.));
#36332=CARTESIAN_POINT('',(-36.5,-9.5,1.));
#36333=CARTESIAN_POINT('',(-36.5,-9.5,1.));
#36334=CARTESIAN_POINT('',(-36.5,11.5,1.));
#36335=CARTESIAN_POINT('',(-36.5,-11.5,-4.));
#36336=CARTESIAN_POINT('',(-36.5,11.5,-4.));
#36337=CARTESIAN_POINT('',(-36.5,-11.5,4.));
#36338=CARTESIAN_POINT('Origin',(-36.5,-11.5,4.));
#36339=CARTESIAN_POINT('',(16.5,-11.5,1.));
#36340=CARTESIAN_POINT('',(16.5,-11.5,1.));
#36341=CARTESIAN_POINT('',(16.5,-11.5,4.));
#36342=CARTESIAN_POINT('',(16.5,-11.5,1.));
#36343=CARTESIAN_POINT('',(-36.5,-11.5,4.));
#36344=CARTESIAN_POINT('',(-36.5,-11.5,-4.));
#36345=CARTESIAN_POINT('Origin',(0.,0.,4.));
#36346=CARTESIAN_POINT('',(16.5,-9.5,4.));
#36347=CARTESIAN_POINT('',(16.5,-9.5,4.));
#36348=CARTESIAN_POINT('',(-36.5,-9.5,4.));
#36349=CARTESIAN_POINT('Origin',(0.,0.,-4.));
#36350=CARTESIAN_POINT('Origin',(34.,11.5,1.));
#36351=CARTESIAN_POINT('',(34.,-1.5,1.));
#36352=CARTESIAN_POINT('',(34.,11.5,1.));
#36353=CARTESIAN_POINT('',(34.,-1.5,1.));
#36354=CARTESIAN_POINT('Origin',(34.,-1.5,1.));
#36355=CARTESIAN_POINT('',(34.,-1.5,1.));
#36356=CARTESIAN_POINT('Origin',(16.5,-9.5,1.));
#36357=CARTESIAN_POINT('',(16.5,-9.5,1.));
#36358=CARTESIAN_POINT('',(16.5,-9.5,1.));
#36359=CARTESIAN_POINT('',(16.5,-9.5,1.));
#36360=CARTESIAN_POINT('Origin',(-36.5,-9.5,1.));
#36361=CARTESIAN_POINT('',(-36.5,-9.5,1.));
#36362=CARTESIAN_POINT('Origin',(0.,0.,1.));
#66643=UNCERTAINTY_MEASURE_WITH_UNIT(LENGTH_MEASURE(0.01),#66722,
'DISTANCE_ACCURACY_VALUE',
'Maximum model space distance between geometric entities at asserted c
onnectivities');
#66680=UNCERTAINTY_MEASURE_WITH_UNIT(LENGTH_MEASURE(0.01),#66722,
'DISTANCE_ACCURACY_VALUE',
'Maximum model space distance between geometric entities at asserted c
onnectivities');
#66684=(
GEOMETRIC_REPRESENTATION_CONTEXT(3)
GLOBAL_UNCERTAINTY_ASSIGNED_CONTEXT((#66643))
GLOBAL_UNIT_ASSIGNED_CONTEXT((#66722,#66724,#66725))
REPRESENTATION_CONTEXT('','3D')
);
#66721=(
GEOMETRIC_REPRESENTATION_CONTEXT(3)
GLOBAL_UNCERTAINTY_ASSIGNED_CONTEXT((#66680))
GLOBAL_UNIT_ASSIGNED_CONTEXT((#66722,#66724,#66725))
REPRESENTATION_CONTEXT('','3D')
);
#66722=(
LENGTH_UNIT()
NAMED_UNIT(*)
SI_UNIT(.MILLI.,.METRE.)
);
#66724=(
NAMED_UNIT(*)
PLANE_ANGLE_UNIT()
SI_UNIT($,.RADIAN.)
);
#66725=(
NAMED_UNIT(*)
SI_UNIT($,.STERADIAN.)
SOLID_ANGLE_UNIT()
);
#66729=SHAPE_DEFINITION_REPRESENTATION(#66769,#66893);
#66769=PRODUCT_DEFINITION_SHAPE('',$,#66934);
#66893=SHAPE_REPRESENTATION('',(#26070),#66684);
#66930=PRODUCT_DEFINITION_CONTEXT('part definition',#67052,'design');
#66934=PRODUCT_DEFINITION('Ball Screw Spacer 2','Ball Screw Spacer 2',#66974,
#66930);
#66974=PRODUCT_DEFINITION_FORMATION('',$,#67057);
#67052=APPLICATION_CONTEXT(
'Core Data for Automotive Mechanical Design Process');
#67053=PRODUCT_CONTEXT('part definition',#67052,'mechanical');
#67057=PRODUCT('Ball Screw Spacer 2','Ball Screw Spacer 2',$,(#67053));
#67095=PRESENTATION_STYLE_ASSIGNMENT((#67097));
#67097=SURFACE_STYLE_USAGE(.BOTH.,#67099);
#67099=SURFACE_SIDE_STYLE('',(#67101));
#67101=SURFACE_STYLE_FILL_AREA(#67103);
#67103=FILL_AREA_STYLE('Opaque(202,209,238)',(#67105));
#67105=FILL_AREA_STYLE_COLOUR('Opaque(202,209,238)',#67107);
#67107=COLOUR_RGB('Opaque(202,209,238)',0.792156862745098,0.819607843137255,
0.933333333333333);
ENDSEC;
END-ISO-10303-21;
